ISO-10303-21;
HEADER;
/* Generated by software containing ST-Developer
 * from STEP Tools, Inc. (www.steptools.com) 
 */

FILE_DESCRIPTION(
/* description */ ('Ball-type isolation valve (generic)'),
/* implementation_level */ '2;1');

FILE_NAME(
/* name */ 'Bridge spacer (1).step',
/* time_stamp */ '2026-10-27T10:53:05-07:00',
/* author */ (''),
/* organization */ (''),
/* preprocessor_version */ 'ST-DEVELOPER v20.2',
/* originating_system */ 'Autodesk Translation Framework v15.17.0.0',
/* authorisation */ '');

FILE_SCHEMA (('AUTOMOTIVE_DESIGN { 1 0 10303 214 3 1 1 }'));
ENDSEC;

DATA;
#10=MECHANICAL_DESIGN_GEOMETRIC_PRESENTATION_REPRESENTATION('',(#287),#7425);
#235=SHAPE_REPRESENTATION_RELATIONSHIP('SRR','None',#7545,#261);
#261=ADVANCED_BREP_SHAPE_REPRESENTATION('',(#313),#7408);
#287=STYLED_ITEM('',(#7737),#313);
#313=MANIFOLD_SOLID_BREP('Body1',#4092);
#393=FACE_BOUND('',#993,.T.);
#394=FACE_BOUND('',#995,.T.);
#472=PLANE('',#4611);
#473=PLANE('',#4612);
#679=FACE_OUTER_BOUND('',#990,.T.);
#680=FACE_OUTER_BOUND('',#991,.T.);
#681=FACE_OUTER_BOUND('',#992,.T.);
#682=FACE_OUTER_BOUND('',#994,.T.);
#990=EDGE_LOOP('',(#3189,#3190,#3191,#3192));
#991=EDGE_LOOP('',(#3193,#3194,#3195,#3196));
#992=EDGE_LOOP('',(#3197));
#993=EDGE_LOOP('',(#3198));
#994=EDGE_LOOP('',(#3199));
#995=EDGE_LOOP('',(#3200));
#1278=LINE('',#6663,#1586);
#1279=LINE('',#6669,#1587);
#1586=VECTOR('',#5427,0.225);
#1587=VECTOR('',#5434,0.4);
#1875=CIRCLE('',#4606,0.225);
#1876=CIRCLE('',#4607,0.225);
#1877=CIRCLE('',#4609,0.4);
#1878=CIRCLE('',#4610,0.4);
#2095=VERTEX_POINT('',#6660);
#2096=VERTEX_POINT('',#6662);
#2097=VERTEX_POINT('',#6666);
#2098=VERTEX_POINT('',#6668);
#2487=EDGE_CURVE('',#2095,#2095,#1875,.T.);
#2488=EDGE_CURVE('',#2095,#2096,#1278,.T.);
#2489=EDGE_CURVE('',#2096,#2096,#1876,.T.);
#2490=EDGE_CURVE('',#2097,#2097,#1877,.T.);
#2491=EDGE_CURVE('',#2097,#2098,#1279,.T.);
#2492=EDGE_CURVE('',#2098,#2098,#1878,.T.);
#3189=ORIENTED_EDGE('',*,*,#2487,.F.);
#3190=ORIENTED_EDGE('',*,*,#2488,.T.);
#3191=ORIENTED_EDGE('',*,*,#2489,.T.);
#3192=ORIENTED_EDGE('',*,*,#2488,.F.);
#3193=ORIENTED_EDGE('',*,*,#2490,.F.);
#3194=ORIENTED_EDGE('',*,*,#2491,.T.);
#3195=ORIENTED_EDGE('',*,*,#2492,.T.);
#3196=ORIENTED_EDGE('',*,*,#2491,.F.);
#3197=ORIENTED_EDGE('',*,*,#2490,.T.);
#3198=ORIENTED_EDGE('',*,*,#2487,.T.);
#3199=ORIENTED_EDGE('',*,*,#2492,.F.);
#3200=ORIENTED_EDGE('',*,*,#2489,.F.);
#3807=CYLINDRICAL_SURFACE('',#4605,0.225);
#3808=CYLINDRICAL_SURFACE('',#4608,0.4);
#3933=ADVANCED_FACE('',(#679),#3807,.F.);
#3934=ADVANCED_FACE('',(#680),#3808,.T.);
#3935=ADVANCED_FACE('',(#681,#393),#472,.T.);
#3936=ADVANCED_FACE('',(#682,#394),#473,.F.);
#4092=CLOSED_SHELL('',(#3933,#3934,#3935,#3936));
#4604=AXIS2_PLACEMENT_3D('',#6658,#5421,#5422);
#4605=AXIS2_PLACEMENT_3D('',#6659,#5423,#5424);
#4606=AXIS2_PLACEMENT_3D('',#6661,#5425,#5426);
#4607=AXIS2_PLACEMENT_3D('',#6664,#5428,#5429);
#4608=AXIS2_PLACEMENT_3D('',#6665,#5430,#5431);
#4609=AXIS2_PLACEMENT_3D('',#6667,#5432,#5433);
#4610=AXIS2_PLACEMENT_3D('',#6670,#5435,#5436);
#4611=AXIS2_PLACEMENT_3D('',#6671,#5437,#5438);
#4612=AXIS2_PLACEMENT_3D('',#6672,#5439,#5440);
#5421=DIRECTION('axis',(0.,0.,1.));
#5422=DIRECTION('refdir',(1.,0.,0.));
#5423=DIRECTION('center_axis',(0.,0.,1.));
#5424=DIRECTION('ref_axis',(1.,0.,0.));
#5425=DIRECTION('center_axis',(0.,0.,-1.));
#5426=DIRECTION('ref_axis',(1.,0.,0.));
#5427=DIRECTION('',(0.,0.,-1.));
#5428=DIRECTION('center_axis',(0.,0.,-1.));
#5429=DIRECTION('ref_axis',(1.,0.,0.));
#5430=DIRECTION('center_axis',(0.,0.,1.));
#5431=DIRECTION('ref_axis',(1.,0.,0.));
#5432=DIRECTION('center_axis',(0.,0.,1.));
#5433=DIRECTION('ref_axis',(1.,0.,0.));
#5434=DIRECTION('',(0.,0.,-1.));
#5435=DIRECTION('center_axis',(0.,0.,1.));
#5436=DIRECTION('ref_axis',(1.,0.,0.));
#5437=DIRECTION('center_axis',(0.,0.,1.));
#5438=DIRECTION('ref_axis',(1.,0.,0.));
#5439=DIRECTION('center_axis',(0.,0.,1.));
#5440=DIRECTION('ref_axis',(1.,0.,0.));
#6658=CARTESIAN_POINT('',(0.,0.,0.));
#6659=CARTESIAN_POINT('Origin',(-1.3,1.,7.5));
#6660=CARTESIAN_POINT('',(-1.525,1.,8.));
#6661=CARTESIAN_POINT('Origin',(-1.3,1.,8.));
#6662=CARTESIAN_POINT('',(-1.525,1.,7.5));
#6663=CARTESIAN_POINT('',(-1.525,1.,7.5));
#6664=CARTESIAN_POINT('Origin',(-1.3,1.,7.5));
#6665=CARTESIAN_POINT('Origin',(-1.3,1.,7.5));
#6666=CARTESIAN_POINT('',(-1.7,1.,8.));
#6667=CARTESIAN_POINT('Origin',(-1.3,1.,8.));
#6668=CARTESIAN_POINT('',(-1.7,1.,7.5));
#6669=CARTESIAN_POINT('',(-1.7,1.,7.5));
#6670=CARTESIAN_POINT('Origin',(-1.3,1.,7.5));
#6671=CARTESIAN_POINT('Origin',(-1.3,1.,8.));
#6672=CARTESIAN_POINT('Origin',(-1.3,1.,7.5));
#7378=UNCERTAINTY_MEASURE_WITH_UNIT(LENGTH_MEASURE(0.001),#7426,
'DISTANCE_ACCURACY_VALUE',
'Maximum model space distance between geometric entities at asserted c
onnectivities');
#7395=UNCERTAINTY_MEASURE_WITH_UNIT(LENGTH_MEASURE(0.001),#7426,
'DISTANCE_ACCURACY_VALUE',
'Maximum model space distance between geometric entities at asserted c
onnectivities');
#7408=(
GEOMETRIC_REPRESENTATION_CONTEXT(3)
GLOBAL_UNCERTAINTY_ASSIGNED_CONTEXT((#7378))
GLOBAL_UNIT_ASSIGNED_CONTEXT((#7426,#7428,#7429))
REPRESENTATION_CONTEXT('','3D')
);
#7425=(
GEOMETRIC_REPRESENTATION_CONTEXT(3)
GLOBAL_UNCERTAINTY_ASSIGNED_CONTEXT((#7395))
GLOBAL_UNIT_ASSIGNED_CONTEXT((#7426,#7428,#7429))
REPRESENTATION_CONTEXT('','3D')
);
#7426=(
LENGTH_UNIT()
NAMED_UNIT(*)
SI_UNIT(.CENTI.,.METRE.)
);
#7428=(
NAMED_UNIT(*)
PLANE_ANGLE_UNIT()
SI_UNIT($,.RADIAN.)
);
#7429=(
NAMED_UNIT(*)
SI_UNIT($,.STERADIAN.)
SOLID_ANGLE_UNIT()
);
#7442=SHAPE_DEFINITION_REPRESENTATION(#7471,#7545);
#7471=PRODUCT_DEFINITION_SHAPE('',$,#7575);
#7545=SHAPE_REPRESENTATION('',(#4604),#7408);
#7562=PRODUCT_DEFINITION_CONTEXT('part definition',#7651,'design');
#7575=PRODUCT_DEFINITION('Bridge spacer (1)','Bridge spacer (1)',#7604,#7562);
#7604=PRODUCT_DEFINITION_FORMATION('',$,#7665);
#7651=APPLICATION_CONTEXT(
'Core Data for Automotive Mechanical Design Process');
#7652=PRODUCT_CONTEXT('part definition',#7651,'mechanical');
#7665=PRODUCT('Bridge spacer (1)','Bridge spacer (1)','Bridge spacer (1)',(#7652));
#7731=COLOUR_RGB('Sky Blue',0.24,0.69,0.87);
#7732=FILL_AREA_STYLE_COLOUR('',#7731);
#7733=FILL_AREA_STYLE('',(#7732));
#7734=SURFACE_STYLE_FILL_AREA(#7733);
#7735=SURFACE_SIDE_STYLE('',(#7734));
#7736=SURFACE_STYLE_USAGE(.BOTH.,#7735);
#7737=PRESENTATION_STYLE_ASSIGNMENT((#7736));
ENDSEC;
END-ISO-10303-21;
